ISO-10303-21;
HEADER;
/* Generated by software containing ST-Developer
 * from STEP Tools, Inc. (www.steptools.com) 
 */

FILE_DESCRIPTION(
/* description */ ('PAT-083'),
/* implementation_level */ '2;1');

FILE_NAME(
/* name */ 'Adjuster knob.step',
/* time_stamp */ '2026-10-29T20:18:00-07:00',
/* author */ (''),
/* organization */ (''),
/* preprocessor_version */ 'ST-DEVELOPER v20.2',
/* originating_system */ 'Autodesk Translation Framework v15.17.0.0',
/* authorisation */ '');

FILE_SCHEMA (('AUTOMOTIVE_DESIGN { 1 0 10303 214 3 1 1 }'));
ENDSEC;

DATA;
#10=MECHANICAL_DESIGN_GEOMETRIC_PRESENTATION_REPRESENTATION('',(#244),#8428);
#178=B_SPLINE_CURVE_WITH_KNOTS('',3,(#7865,#7866,#7867,#7868,#7869,#7870,
#7871,#7872,#7873,#7874),.UNSPECIFIED.,.F.,.F.,(4,2,2,2,4),(0.665271585430993,
0.692803751398642,0.755746158887619,0.818688566376595,0.846220732344244),
 .UNSPECIFIED.);
#179=B_SPLINE_CURVE_WITH_KNOTS('',3,(#7877,#7878,#7879,#7880,#7881,#7882,
#7883,#7884,#7885,#7886),.UNSPECIFIED.,.F.,.F.,(4,2,2,2,4),(0.161440812839248,
0.188972978806896,0.251915386295873,0.314857793784849,0.342389959752498),
 .UNSPECIFIED.);
#180=B_SPLINE_CURVE_WITH_KNOTS('',3,(#7889,#7890,#7891,#7892,#7893,#7894,
#7895,#7896,#7897,#7898,#7899,#7900,#7901,#7902,#7903,#7904,#7905,#7906,
#7907,#7908,#7909,#7910,#7911,#7912,#7913,#7914,#7915,#7916,#7917,#7918,
#7919,#7920,#7921,#7922),.UNSPECIFIED.,.T.,.F.,(4,2,2,2,2,2,2,2,2,2,2,2,
2,2,2,2,4),(0.,0.0622075173149514,0.124415034629903,0.186622241324509,0.248829448019115,
0.311036654713721,0.373243861408326,0.435451378723278,0.497658896038229,
0.559866413353181,0.622073930668132,0.684281137362738,0.746488344057344,
0.80869555075195,0.870902757446556,0.933110274761507,0.995317792076459),
 .UNSPECIFIED.);
#196=SHAPE_REPRESENTATION_RELATIONSHIP('SRR','None',#8530,#220);
#220=ADVANCED_BREP_SHAPE_REPRESENTATION('',(#268),#8419);
#244=STYLED_ITEM('',(#8691),#268);
#268=MANIFOLD_SOLID_BREP('Body1',#3690);
#341=FACE_BOUND('',#936,.T.);
#342=FACE_BOUND('',#938,.T.);
#343=FACE_BOUND('',#940,.T.);
#344=FACE_BOUND('',#942,.T.);
#428=PLANE('',#4259);
#429=PLANE('',#4264);
#430=PLANE('',#4271);
#431=PLANE('',#4272);
#633=FACE_OUTER_BOUND('',#932,.T.);
#634=FACE_OUTER_BOUND('',#933,.T.);
#635=FACE_OUTER_BOUND('',#934,.T.);
#636=FACE_OUTER_BOUND('',#935,.T.);
#637=FACE_OUTER_BOUND('',#937,.T.);
#638=FACE_OUTER_BOUND('',#939,.T.);
#639=FACE_OUTER_BOUND('',#941,.T.);
#932=EDGE_LOOP('',(#2984,#2985,#2986));
#933=EDGE_LOOP('',(#2987,#2988,#2989,#2990,#2991,#2992,#2993,#2994));
#934=EDGE_LOOP('',(#2995,#2996));
#935=EDGE_LOOP('',(#2997,#2998,#2999,#3000));
#936=EDGE_LOOP('',(#3001,#3002,#3003,#3004));
#937=EDGE_LOOP('',(#3005,#3006,#3007,#3008));
#938=EDGE_LOOP('',(#3009));
#939=EDGE_LOOP('',(#3010));
#940=EDGE_LOOP('',(#3011));
#941=EDGE_LOOP('',(#3012));
#942=EDGE_LOOP('',(#3013));
#1154=LINE('',#7859,#1398);
#1155=LINE('',#7888,#1399);
#1156=LINE('',#7924,#1400);
#1157=LINE('',#7929,#1401);
#1158=LINE('',#7935,#1402);
#1398=VECTOR('',#5136,1.);
#1399=VECTOR('',#5145,0.165);
#1400=VECTOR('',#5148,1.);
#1401=VECTOR('',#5153,0.4);
#1402=VECTOR('',#5160,1.5);
#1670=CIRCLE('',#4260,0.165);
#1671=CIRCLE('',#4261,0.165);
#1672=CIRCLE('',#4263,0.165);
#1673=CIRCLE('',#4266,0.4);
#1674=CIRCLE('',#4267,0.4);
#1675=CIRCLE('',#4269,1.5);
#1676=CIRCLE('',#4270,1.5);
#1883=VERTEX_POINT('',#7857);
#1884=VERTEX_POINT('',#7858);
#1885=VERTEX_POINT('',#7860);
#1886=VERTEX_POINT('',#7864);
#1887=VERTEX_POINT('',#7875);
#1888=VERTEX_POINT('',#7887);
#1889=VERTEX_POINT('',#7926);
#1890=VERTEX_POINT('',#7928);
#1891=VERTEX_POINT('',#7932);
#1892=VERTEX_POINT('',#7934);
#2268=EDGE_CURVE('',#1883,#1884,#1154,.T.);
#2269=EDGE_CURVE('',#1883,#1885,#1670,.T.);
#2270=EDGE_CURVE('',#1885,#1884,#1671,.T.);
#2271=EDGE_CURVE('',#1886,#1883,#178,.T.);
#2272=EDGE_CURVE('',#1887,#1886,#1672,.T.);
#2273=EDGE_CURVE('',#1884,#1887,#179,.T.);
#2274=EDGE_CURVE('',#1885,#1888,#1155,.T.);
#2275=EDGE_CURVE('',#1888,#1888,#180,.T.);
#2276=EDGE_CURVE('',#1887,#1886,#1156,.T.);
#2277=EDGE_CURVE('',#1889,#1889,#1673,.T.);
#2278=EDGE_CURVE('',#1889,#1890,#1157,.T.);
#2279=EDGE_CURVE('',#1890,#1890,#1674,.T.);
#2280=EDGE_CURVE('',#1891,#1891,#1675,.T.);
#2281=EDGE_CURVE('',#1891,#1892,#1158,.T.);
#2282=EDGE_CURVE('',#1892,#1892,#1676,.T.);
#2984=ORIENTED_EDGE('',*,*,#2268,.F.);
#2985=ORIENTED_EDGE('',*,*,#2269,.T.);
#2986=ORIENTED_EDGE('',*,*,#2270,.T.);
#2987=ORIENTED_EDGE('',*,*,#2271,.F.);
#2988=ORIENTED_EDGE('',*,*,#2272,.F.);
#2989=ORIENTED_EDGE('',*,*,#2273,.F.);
#2990=ORIENTED_EDGE('',*,*,#2270,.F.);
#2991=ORIENTED_EDGE('',*,*,#2274,.T.);
#2992=ORIENTED_EDGE('',*,*,#2275,.F.);
#2993=ORIENTED_EDGE('',*,*,#2274,.F.);
#2994=ORIENTED_EDGE('',*,*,#2269,.F.);
#2995=ORIENTED_EDGE('',*,*,#2276,.F.);
#2996=ORIENTED_EDGE('',*,*,#2272,.T.);
#2997=ORIENTED_EDGE('',*,*,#2277,.F.);
#2998=ORIENTED_EDGE('',*,*,#2278,.T.);
#2999=ORIENTED_EDGE('',*,*,#2279,.T.);
#3000=ORIENTED_EDGE('',*,*,#2278,.F.);
#3001=ORIENTED_EDGE('',*,*,#2273,.T.);
#3002=ORIENTED_EDGE('',*,*,#2276,.T.);
#3003=ORIENTED_EDGE('',*,*,#2271,.T.);
#3004=ORIENTED_EDGE('',*,*,#2268,.T.);
#3005=ORIENTED_EDGE('',*,*,#2280,.F.);
#3006=ORIENTED_EDGE('',*,*,#2281,.T.);
#3007=ORIENTED_EDGE('',*,*,#2282,.T.);
#3008=ORIENTED_EDGE('',*,*,#2281,.F.);
#3009=ORIENTED_EDGE('',*,*,#2275,.T.);
#3010=ORIENTED_EDGE('',*,*,#2280,.T.);
#3011=ORIENTED_EDGE('',*,*,#2277,.T.);
#3012=ORIENTED_EDGE('',*,*,#2282,.F.);
#3013=ORIENTED_EDGE('',*,*,#2279,.F.);
#3428=CYLINDRICAL_SURFACE('',#4262,0.165);
#3429=CYLINDRICAL_SURFACE('',#4265,0.4);
#3430=CYLINDRICAL_SURFACE('',#4268,1.5);
#3580=ADVANCED_FACE('',(#633),#428,.T.);
#3581=ADVANCED_FACE('',(#634),#3428,.F.);
#3582=ADVANCED_FACE('',(#635),#429,.T.);
#3583=ADVANCED_FACE('',(#636,#341),#3429,.F.);
#3584=ADVANCED_FACE('',(#637,#342),#3430,.T.);
#3585=ADVANCED_FACE('',(#638,#343),#430,.T.);
#3586=ADVANCED_FACE('',(#639,#344),#431,.F.);
#3690=CLOSED_SHELL('',(#3580,#3581,#3582,#3583,#3584,#3585,#3586));
#4258=AXIS2_PLACEMENT_3D('',#7855,#5132,#5133);
#4259=AXIS2_PLACEMENT_3D('',#7856,#5134,#5135);
#4260=AXIS2_PLACEMENT_3D('',#7861,#5137,#5138);
#4261=AXIS2_PLACEMENT_3D('',#7862,#5139,#5140);
#4262=AXIS2_PLACEMENT_3D('',#7863,#5141,#5142);
#4263=AXIS2_PLACEMENT_3D('',#7876,#5143,#5144);
#4264=AXIS2_PLACEMENT_3D('',#7923,#5146,#5147);
#4265=AXIS2_PLACEMENT_3D('',#7925,#5149,#5150);
#4266=AXIS2_PLACEMENT_3D('',#7927,#5151,#5152);
#4267=AXIS2_PLACEMENT_3D('',#7930,#5154,#5155);
#4268=AXIS2_PLACEMENT_3D('',#7931,#5156,#5157);
#4269=AXIS2_PLACEMENT_3D('',#7933,#5158,#5159);
#4270=AXIS2_PLACEMENT_3D('',#7936,#5161,#5162);
#4271=AXIS2_PLACEMENT_3D('',#7937,#5163,#5164);
#4272=AXIS2_PLACEMENT_3D('',#7938,#5165,#5166);
#5132=DIRECTION('axis',(0.,0.,1.));
#5133=DIRECTION('refdir',(1.,0.,0.));
#5134=DIRECTION('center_axis',(0.,1.,0.));
#5135=DIRECTION('ref_axis',(1.,0.,0.));
#5136=DIRECTION('',(0.,0.,1.));
#5137=DIRECTION('center_axis',(0.,1.,0.));
#5138=DIRECTION('ref_axis',(1.,0.,0.));
#5139=DIRECTION('center_axis',(0.,1.,0.));
#5140=DIRECTION('ref_axis',(1.,0.,0.));
#5141=DIRECTION('center_axis',(0.,1.,0.));
#5142=DIRECTION('ref_axis',(1.,0.,0.));
#5143=DIRECTION('center_axis',(0.,1.,0.));
#5144=DIRECTION('ref_axis',(1.,0.,0.));
#5145=DIRECTION('',(0.,1.,0.));
#5146=DIRECTION('center_axis',(0.,1.,0.));
#5147=DIRECTION('ref_axis',(1.,0.,0.));
#5148=DIRECTION('',(0.,0.,-1.));
#5149=DIRECTION('center_axis',(0.,0.,1.));
#5150=DIRECTION('ref_axis',(1.,0.,0.));
#5151=DIRECTION('center_axis',(0.,0.,-1.));
#5152=DIRECTION('ref_axis',(1.,0.,0.));
#5153=DIRECTION('',(0.,0.,-1.));
#5154=DIRECTION('center_axis',(0.,0.,-1.));
#5155=DIRECTION('ref_axis',(1.,0.,0.));
#5156=DIRECTION('center_axis',(0.,0.,1.));
#5157=DIRECTION('ref_axis',(1.,0.,0.));
#5158=DIRECTION('center_axis',(0.,0.,1.));
#5159=DIRECTION('ref_axis',(1.,0.,0.));
#5160=DIRECTION('',(0.,0.,-1.));
#5161=DIRECTION('center_axis',(0.,0.,1.));
#5162=DIRECTION('ref_axis',(1.,0.,0.));
#5163=DIRECTION('center_axis',(0.,0.,1.));
#5164=DIRECTION('ref_axis',(1.,0.,0.));
#5165=DIRECTION('center_axis',(0.,0.,1.));
#5166=DIRECTION('ref_axis',(1.,0.,0.));
#7855=CARTESIAN_POINT('',(0.,0.,0.));
#7856=CARTESIAN_POINT('Origin',(0.,0.39,11.));
#7857=CARTESIAN_POINT('',(-0.088881944173156,0.39,10.8609856122554));
#7858=CARTESIAN_POINT('',(-0.088881944173156,0.39,11.1390143877446));
#7859=CARTESIAN_POINT('',(-0.088881944173156,0.39,10.5));
#7860=CARTESIAN_POINT('',(-0.165,0.39,11.));
#7861=CARTESIAN_POINT('Origin',(0.,0.39,11.));
#7862=CARTESIAN_POINT('Origin',(0.,0.39,11.));
#7863=CARTESIAN_POINT('Origin',(0.,0.39,11.));
#7864=CARTESIAN_POINT('',(0.088881944173156,0.39,10.8609856122554));
#7865=CARTESIAN_POINT('Ctrl Pts',(0.088881944173156,0.39,10.8609856122554));
#7866=CARTESIAN_POINT('Ctrl Pts',(0.0808964434200154,0.391819914954193,
10.8558799045395));
#7867=CARTESIAN_POINT('Ctrl Pts',(0.072364333302368,0.393502517883282,10.8514036081398));
#7868=CARTESIAN_POINT('Ctrl Pts',(0.0431949313468624,0.398191715532106,
10.8392437758303));
#7869=CARTESIAN_POINT('Ctrl Pts',(0.0209808024963256,0.4,10.835));
#7870=CARTESIAN_POINT('Ctrl Pts',(-0.0209808024963256,0.4,10.835));
#7871=CARTESIAN_POINT('Ctrl Pts',(-0.0431949313468624,0.398191715532106,
10.8392437758303));
#7872=CARTESIAN_POINT('Ctrl Pts',(-0.072364333302368,0.393502517883282,
10.8514036081398));
#7873=CARTESIAN_POINT('Ctrl Pts',(-0.0808964434200154,0.391819914954193,
10.8558799045395));
#7874=CARTESIAN_POINT('Ctrl Pts',(-0.088881944173156,0.39,10.8609856122554));
#7875=CARTESIAN_POINT('',(0.088881944173156,0.39,11.1390143877446));
#7876=CARTESIAN_POINT('Origin',(0.,0.39,11.));
#7877=CARTESIAN_POINT('Ctrl Pts',(-0.088881944173156,0.39,11.1390143877446));
#7878=CARTESIAN_POINT('Ctrl Pts',(-0.0808964434200154,0.391819914954193,
11.1441200954605));
#7879=CARTESIAN_POINT('Ctrl Pts',(-0.072364333302368,0.393502517883282,
11.1485963918602));
#7880=CARTESIAN_POINT('Ctrl Pts',(-0.0431949313468623,0.398191715532106,
11.1607562241697));
#7881=CARTESIAN_POINT('Ctrl Pts',(-0.0209808024963255,0.4,11.165));
#7882=CARTESIAN_POINT('Ctrl Pts',(0.0209808024963256,0.4,11.165));
#7883=CARTESIAN_POINT('Ctrl Pts',(0.0431949313468623,0.398191715532106,
11.1607562241697));
#7884=CARTESIAN_POINT('Ctrl Pts',(0.072364333302368,0.393502517883282,11.1485963918602));
#7885=CARTESIAN_POINT('Ctrl Pts',(0.0808964434200153,0.391819914954193,
11.1441200954605));
#7886=CARTESIAN_POINT('Ctrl Pts',(0.088881944173156,0.39,11.1390143877446));
#7887=CARTESIAN_POINT('',(-0.165,1.49089738077441,11.));
#7888=CARTESIAN_POINT('',(-0.165,0.39,11.));
#7889=CARTESIAN_POINT('Ctrl Pts',(-0.165,1.49089738077441,11.));
#7890=CARTESIAN_POINT('Ctrl Pts',(-0.165,1.49089738077441,10.979264160895));
#7891=CARTESIAN_POINT('Ctrl Pts',(-0.160852499025073,1.49137458218466,10.9571577290991));
#7892=CARTESIAN_POINT('Ctrl Pts',(-0.144008447160944,1.49309518705251,10.916510155069));
#7893=CARTESIAN_POINT('Ctrl Pts',(-0.131312810193433,1.49431341615515,10.8979675724019));
#7894=CARTESIAN_POINT('Ctrl Pts',(-0.102032500700889,1.49659781052539,10.8686872629093));
#7895=CARTESIAN_POINT('Ctrl Pts',(-0.0834898860986569,1.49781281581157,
10.8559915687804));
#7896=CARTESIAN_POINT('Ctrl Pts',(-0.042842204593242,1.49952603771524,10.8391474746158));
#7897=CARTESIAN_POINT('Ctrl Pts',(-0.0207357355648686,1.5,10.835));
#7898=CARTESIAN_POINT('Ctrl Pts',(0.0207357355648686,1.5,10.835));
#7899=CARTESIAN_POINT('Ctrl Pts',(0.0428422045932419,1.49952603771524,10.8391474746158));
#7900=CARTESIAN_POINT('Ctrl Pts',(0.0834898860986569,1.49781281581157,10.8559915687804));
#7901=CARTESIAN_POINT('Ctrl Pts',(0.102032500700889,1.49659781052539,10.8686872629093));
#7902=CARTESIAN_POINT('Ctrl Pts',(0.131312810193433,1.49431341615515,10.8979675724019));
#7903=CARTESIAN_POINT('Ctrl Pts',(0.144008447160944,1.49309518705251,10.916510155069));
#7904=CARTESIAN_POINT('Ctrl Pts',(0.160852499025073,1.49137458218466,10.9571577290991));
#7905=CARTESIAN_POINT('Ctrl Pts',(0.165,1.49089738077441,10.979264160895));
#7906=CARTESIAN_POINT('Ctrl Pts',(0.165,1.49089738077441,11.020735839105));
#7907=CARTESIAN_POINT('Ctrl Pts',(0.160852499025073,1.49137458218466,11.0428422709009));
#7908=CARTESIAN_POINT('Ctrl Pts',(0.144008447160944,1.49309518705251,11.083489844931));
#7909=CARTESIAN_POINT('Ctrl Pts',(0.131312810193433,1.49431341615515,11.1020324275981));
#7910=CARTESIAN_POINT('Ctrl Pts',(0.102032500700889,1.49659781052539,11.1313127370907));
#7911=CARTESIAN_POINT('Ctrl Pts',(0.0834898860986569,1.49781281581157,11.1440084312196));
#7912=CARTESIAN_POINT('Ctrl Pts',(0.042842204593242,1.49952603771524,11.1608525253842));
#7913=CARTESIAN_POINT('Ctrl Pts',(0.0207357355648686,1.5,11.165));
#7914=CARTESIAN_POINT('Ctrl Pts',(-0.0207357355648686,1.5,11.165));
#7915=CARTESIAN_POINT('Ctrl Pts',(-0.0428422045932419,1.49952603771524,
11.1608525253842));
#7916=CARTESIAN_POINT('Ctrl Pts',(-0.0834898860986569,1.49781281581157,
11.1440084312196));
#7917=CARTESIAN_POINT('Ctrl Pts',(-0.102032500700889,1.49659781052539,11.1313127370907));
#7918=CARTESIAN_POINT('Ctrl Pts',(-0.131312810193433,1.49431341615515,11.1020324275981));
#7919=CARTESIAN_POINT('Ctrl Pts',(-0.144008447160944,1.49309518705251,11.083489844931));
#7920=CARTESIAN_POINT('Ctrl Pts',(-0.160852499025073,1.49137458218466,11.0428422709009));
#7921=CARTESIAN_POINT('Ctrl Pts',(-0.165,1.49089738077441,11.020735839105));
#7922=CARTESIAN_POINT('Ctrl Pts',(-0.165,1.49089738077441,11.));
#7923=CARTESIAN_POINT('Origin',(0.,0.39,11.));
#7924=CARTESIAN_POINT('',(0.088881944173156,0.39,10.5));
#7925=CARTESIAN_POINT('Origin',(0.,0.,10.5));
#7926=CARTESIAN_POINT('',(-0.4,-4.89858719658941E-17,11.5));
#7927=CARTESIAN_POINT('Origin',(0.,0.,11.5));
#7928=CARTESIAN_POINT('',(-0.4,-4.89858719658941E-17,10.5));
#7929=CARTESIAN_POINT('',(-0.4,-4.89858719658941E-17,10.5));
#7930=CARTESIAN_POINT('Origin',(0.,0.,10.5));
#7931=CARTESIAN_POINT('Origin',(0.,0.,10.5));
#7932=CARTESIAN_POINT('',(-1.5,-1.83697019872103E-16,11.5));
#7933=CARTESIAN_POINT('Origin',(0.,0.,11.5));
#7934=CARTESIAN_POINT('',(-1.5,-1.83697019872103E-16,10.5));
#7935=CARTESIAN_POINT('',(-1.5,-1.83697019872103E-16,10.5));
#7936=CARTESIAN_POINT('Origin',(0.,0.,10.5));
#7937=CARTESIAN_POINT('Origin',(0.,0.,11.5));
#7938=CARTESIAN_POINT('Origin',(0.,0.,10.5));
#8393=UNCERTAINTY_MEASURE_WITH_UNIT(LENGTH_MEASURE(0.001),#8429,
'DISTANCE_ACCURACY_VALUE',
'Maximum model space distance between geometric entities at asserted c
onnectivities');
#8402=UNCERTAINTY_MEASURE_WITH_UNIT(LENGTH_MEASURE(0.001),#8429,
'DISTANCE_ACCURACY_VALUE',
'Maximum model space distance between geometric entities at asserted c
onnectivities');
#8419=(
GEOMETRIC_REPRESENTATION_CONTEXT(3)
GLOBAL_UNCERTAINTY_ASSIGNED_CONTEXT((#8393))
GLOBAL_UNIT_ASSIGNED_CONTEXT((#8429,#8431,#8432))
REPRESENTATION_CONTEXT('','3D')
);
#8428=(
GEOMETRIC_REPRESENTATION_CONTEXT(3)
GLOBAL_UNCERTAINTY_ASSIGNED_CONTEXT((#8402))
GLOBAL_UNIT_ASSIGNED_CONTEXT((#8429,#8431,#8432))
REPRESENTATION_CONTEXT('','3D')
);
#8429=(
LENGTH_UNIT()
NAMED_UNIT(*)
SI_UNIT(.CENTI.,.METRE.)
);
#8431=(
NAMED_UNIT(*)
PLANE_ANGLE_UNIT()
SI_UNIT($,.RADIAN.)
);
#8432=(
NAMED_UNIT(*)
SI_UNIT($,.STERADIAN.)
SOLID_ANGLE_UNIT()
);
#8449=SHAPE_DEFINITION_REPRESENTATION(#8474,#8530);
#8474=PRODUCT_DEFINITION_SHAPE('',$,#8556);
#8530=SHAPE_REPRESENTATION('',(#4258),#8419);
#8539=PRODUCT_DEFINITION_CONTEXT('part definition',#8616,'design');
#8556=PRODUCT_DEFINITION('Adjuster knob','Adjuster knob',#8581,
#8539);
#8581=PRODUCT_DEFINITION_FORMATION('',$,#8634);
#8616=APPLICATION_CONTEXT(
'Core Data for Automotive Mechanical Design Process');
#8617=PRODUCT_CONTEXT('part definition',#8616,'mechanical');
#8634=PRODUCT('Adjuster knob','Adjuster knob',
'Adjuster knob',(#8617));
#8685=COLOUR_RGB('Light Blue',0.38,0.62,0.78);
#8686=FILL_AREA_STYLE_COLOUR('',#8685);
#8687=FILL_AREA_STYLE('',(#8686));
#8688=SURFACE_STYLE_FILL_AREA(#8687);
#8689=SURFACE_SIDE_STYLE('',(#8688));
#8690=SURFACE_STYLE_USAGE(.BOTH.,#8689);
#8691=PRESENTATION_STYLE_ASSIGNMENT((#8690));
ENDSEC;
END-ISO-10303-21;
